ISO-10303-21;
HEADER;
/* Generated by software containing ST-Developer
 * from STEP Tools, Inc. (www.steptools.com) 
 */

FILE_DESCRIPTION(
/* description */ ('Compact handwheel screw vise'),
/* implementation_level */ '2;1');

FILE_NAME(
/* name */ 'Flat Washer - M6.step',
/* time_stamp */ '2026-10-29T16:08:22-07:00',
/* author */ (''),
/* organization */ (''),
/* preprocessor_version */ 'ST-DEVELOPER v20.2',
/* originating_system */ 'Autodesk Translation Framework v15.17.0.0',
/* authorisation */ '');

FILE_SCHEMA (('AUTOMOTIVE_DESIGN { 1 0 10303 214 3 1 1 }'));
ENDSEC;

DATA;
#10=MECHANICAL_DESIGN_GEOMETRIC_PRESENTATION_REPRESENTATION('',(#678),#25074);
#614=SHAPE_REPRESENTATION_RELATIONSHIP('SRR','None',#25225,#642);
#642=ADVANCED_BREP_SHAPE_REPRESENTATION('',(#711),#25072);
#678=STYLED_ITEM('',(#25446),#711);
#711=MANIFOLD_SOLID_BREP('Body1',#8089);
#819=FACE_BOUND('',#2041,.T.);
#820=FACE_BOUND('',#2043,.T.);
#999=PLANE('',#9143);
#1000=PLANE('',#9144);
#1461=FACE_OUTER_BOUND('',#2038,.T.);
#1462=FACE_OUTER_BOUND('',#2039,.T.);
#1463=FACE_OUTER_BOUND('',#2040,.T.);
#1464=FACE_OUTER_BOUND('',#2042,.T.);
#2038=EDGE_LOOP('',(#7269,#7270,#7271,#7272));
#2039=EDGE_LOOP('',(#7273,#7274,#7275,#7276));
#2040=EDGE_LOOP('',(#7277));
#2041=EDGE_LOOP('',(#7278));
#2042=EDGE_LOOP('',(#7279));
#2043=EDGE_LOOP('',(#7280));
#2544=LINE('',#24894,#3052);
#2545=LINE('',#24900,#3053);
#3052=VECTOR('',#11162,0.32);
#3053=VECTOR('',#11169,0.6);
#3321=CIRCLE('',#9138,0.32);
#3322=CIRCLE('',#9139,0.32);
#3323=CIRCLE('',#9141,0.6);
#3324=CIRCLE('',#9142,0.6);
#4042=VERTEX_POINT('',#24891);
#4043=VERTEX_POINT('',#24893);
#4044=VERTEX_POINT('',#24897);
#4045=VERTEX_POINT('',#24899);
#5121=EDGE_CURVE('',#4042,#4042,#3321,.T.);
#5122=EDGE_CURVE('',#4042,#4043,#2544,.T.);
#5123=EDGE_CURVE('',#4043,#4043,#3322,.T.);
#5124=EDGE_CURVE('',#4044,#4044,#3323,.T.);
#5125=EDGE_CURVE('',#4044,#4045,#2545,.T.);
#5126=EDGE_CURVE('',#4045,#4045,#3324,.T.);
#7269=ORIENTED_EDGE('',*,*,#5121,.F.);
#7270=ORIENTED_EDGE('',*,*,#5122,.T.);
#7271=ORIENTED_EDGE('',*,*,#5123,.T.);
#7272=ORIENTED_EDGE('',*,*,#5122,.F.);
#7273=ORIENTED_EDGE('',*,*,#5124,.F.);
#7274=ORIENTED_EDGE('',*,*,#5125,.T.);
#7275=ORIENTED_EDGE('',*,*,#5126,.T.);
#7276=ORIENTED_EDGE('',*,*,#5125,.F.);
#7277=ORIENTED_EDGE('',*,*,#5124,.T.);
#7278=ORIENTED_EDGE('',*,*,#5121,.T.);
#7279=ORIENTED_EDGE('',*,*,#5126,.F.);
#7280=ORIENTED_EDGE('',*,*,#5123,.F.);
#7578=CYLINDRICAL_SURFACE('',#9137,0.32);
#7579=CYLINDRICAL_SURFACE('',#9140,0.6);
#8031=ADVANCED_FACE('',(#1461),#7578,.F.);
#8032=ADVANCED_FACE('',(#1462),#7579,.T.);
#8033=ADVANCED_FACE('',(#1463,#819),#999,.T.);
#8034=ADVANCED_FACE('',(#1464,#820),#1000,.F.);
#8089=CLOSED_SHELL('',(#8031,#8032,#8033,#8034));
#9136=AXIS2_PLACEMENT_3D('',#24889,#11156,#11157);
#9137=AXIS2_PLACEMENT_3D('',#24890,#11158,#11159);
#9138=AXIS2_PLACEMENT_3D('',#24892,#11160,#11161);
#9139=AXIS2_PLACEMENT_3D('',#24895,#11163,#11164);
#9140=AXIS2_PLACEMENT_3D('',#24896,#11165,#11166);
#9141=AXIS2_PLACEMENT_3D('',#24898,#11167,#11168);
#9142=AXIS2_PLACEMENT_3D('',#24901,#11170,#11171);
#9143=AXIS2_PLACEMENT_3D('',#24902,#11172,#11173);
#9144=AXIS2_PLACEMENT_3D('',#24903,#11174,#11175);
#11156=DIRECTION('axis',(0.,0.,1.));
#11157=DIRECTION('refdir',(1.,0.,0.));
#11158=DIRECTION('center_axis',(0.,1.,0.));
#11159=DIRECTION('ref_axis',(1.,0.,0.));
#11160=DIRECTION('center_axis',(0.,-1.,0.));
#11161=DIRECTION('ref_axis',(1.,0.,0.));
#11162=DIRECTION('',(0.,-1.,0.));
#11163=DIRECTION('center_axis',(0.,-1.,0.));
#11164=DIRECTION('ref_axis',(1.,0.,0.));
#11165=DIRECTION('center_axis',(0.,1.,0.));
#11166=DIRECTION('ref_axis',(1.,0.,0.));
#11167=DIRECTION('center_axis',(0.,1.,0.));
#11168=DIRECTION('ref_axis',(1.,0.,0.));
#11169=DIRECTION('',(0.,-1.,0.));
#11170=DIRECTION('center_axis',(0.,1.,0.));
#11171=DIRECTION('ref_axis',(1.,0.,0.));
#11172=DIRECTION('center_axis',(0.,1.,0.));
#11173=DIRECTION('ref_axis',(1.,0.,0.));
#11174=DIRECTION('center_axis',(0.,1.,0.));
#11175=DIRECTION('ref_axis',(1.,0.,0.));
#24889=CARTESIAN_POINT('',(0.,0.,0.));
#24890=CARTESIAN_POINT('Origin',(0.,0.,0.));
#24891=CARTESIAN_POINT('',(-0.32,0.16,3.91886975727153E-17));
#24892=CARTESIAN_POINT('Origin',(0.,0.16,0.));
#24893=CARTESIAN_POINT('',(-0.32,0.,3.91886975727153E-17));
#24894=CARTESIAN_POINT('',(-0.32,0.,3.91886975727153E-17));
#24895=CARTESIAN_POINT('Origin',(0.,0.,0.));
#24896=CARTESIAN_POINT('Origin',(0.,0.,0.));
#24897=CARTESIAN_POINT('',(-0.6,0.16,7.34788079488412E-17));
#24898=CARTESIAN_POINT('Origin',(0.,0.16,0.));
#24899=CARTESIAN_POINT('',(-0.6,0.,7.34788079488412E-17));
#24900=CARTESIAN_POINT('',(-0.6,0.,7.34788079488412E-17));
#24901=CARTESIAN_POINT('Origin',(0.,0.,0.));
#24902=CARTESIAN_POINT('Origin',(0.,0.16,0.));
#24903=CARTESIAN_POINT('Origin',(0.,0.,0.));
#25038=UNCERTAINTY_MEASURE_WITH_UNIT(LENGTH_MEASURE(0.001),#25075,
'DISTANCE_ACCURACY_VALUE',
'Maximum model space distance between geometric entities at asserted c
onnectivities');
#25040=UNCERTAINTY_MEASURE_WITH_UNIT(LENGTH_MEASURE(0.001),#25075,
'DISTANCE_ACCURACY_VALUE',
'Maximum model space distance between geometric entities at asserted c
onnectivities');
#25072=(
GEOMETRIC_REPRESENTATION_CONTEXT(3)
GLOBAL_UNCERTAINTY_ASSIGNED_CONTEXT((#25038))
GLOBAL_UNIT_ASSIGNED_CONTEXT((#25075,#25077,#25078))
REPRESENTATION_CONTEXT('','3D')
);
#25074=(
GEOMETRIC_REPRESENTATION_CONTEXT(3)
GLOBAL_UNCERTAINTY_ASSIGNED_CONTEXT((#25040))
GLOBAL_UNIT_ASSIGNED_CONTEXT((#25075,#25077,#25078))
REPRESENTATION_CONTEXT('','3D')
);
#25075=(
LENGTH_UNIT()
NAMED_UNIT(*)
SI_UNIT(.CENTI.,.METRE.)
);
#25077=(
NAMED_UNIT(*)
PLANE_ANGLE_UNIT()
SI_UNIT($,.RADIAN.)
);
#25078=(
NAMED_UNIT(*)
SI_UNIT($,.STERADIAN.)
SOLID_ANGLE_UNIT()
);
#25110=SHAPE_DEFINITION_REPRESENTATION(#25159,#25225);
#25159=PRODUCT_DEFINITION_SHAPE('',$,#25259);
#25225=SHAPE_REPRESENTATION('',(#9136),#25072);
#25227=PRODUCT_DEFINITION_CONTEXT('part definition',#25328,'design');
#25259=PRODUCT_DEFINITION('Flat Washer - M6','Flat Washer - M6',#25292,
#25227);
#25292=PRODUCT_DEFINITION_FORMATION('',$,#25361);
#25328=APPLICATION_CONTEXT(
'Core Data for Automotive Mechanical Design Process');
#25329=PRODUCT_CONTEXT('part definition',#25328,'mechanical');
#25361=PRODUCT('Flat Washer - M6','Flat Washer - M6','Flat Washer - M6',
(#25329));
#25440=COLOUR_RGB('Black',0.12,0.14,0.17);
#25441=FILL_AREA_STYLE_COLOUR('',#25440);
#25442=FILL_AREA_STYLE('',(#25441));
#25443=SURFACE_STYLE_FILL_AREA(#25442);
#25444=SURFACE_SIDE_STYLE('',(#25443));
#25445=SURFACE_STYLE_USAGE(.BOTH.,#25444);
#25446=PRESENTATION_STYLE_ASSIGNMENT((#25445));
ENDSEC;
END-ISO-10303-21;
